ISO-10303-21;
HEADER;
FILE_DESCRIPTION (('STEP AP203'),
    '1' );
FILE_NAME ('1602p_c_18.step',
    '2026-10-31T14:11:27',
    ( '' ),
    ( '' ),
    'SwSTEP 2.0',
    'SolidWorks 2024',
    '' );
FILE_SCHEMA (( 'AUTOMOTIVE_DESIGN' ));
ENDSEC;

DATA;
#44=FACE_OUTER_BOUND ( 'NONE', #302, .T. ) ;
#45=CYLINDRICAL_SURFACE ( 'NONE', #4982, 2.499999999999998668 ) ;
#120=ORIENTED_EDGE ( 'NONE', *, *, #19486, .F. ) ;
#206=ADVANCED_FACE ( 'NONE', ( #12841 ), #9161, .T. ) ;
#248=DIRECTION ( 'NONE',  ( -6.662111519016958720E-09, 1.000000000000000000, -2.523234146875356491E-15 ) ) ;
#302=EDGE_LOOP ( 'NONE', ( #2041, #9223, #15039, #5086 ) ) ;
#351=EDGE_CURVE ( 'NONE', #2950, #23008, #5497, .T. ) ;
#415=DIRECTION ( 'NONE',  ( 1.000000000000000000, 0.000000000000000000, 0.000000000000000000 ) ) ;
#495=DIRECTION ( 'NONE',  ( -2.979590041760124764E-09, 0.4472135954999595375, -0.8944271909999150783 ) ) ;
#535=ADVANCED_FACE ( 'NONE', ( #23459 ), #3525, .T. ) ;
#608=APPLICATION_CONTEXT ( 'configuration controlled 3d designs of mechanical parts and assemblies' ) ;
#714=CIRCLE ( 'NONE', #20466, 2.749999999999999112 ) ;
#715=CARTESIAN_POINT ( 'NONE',  ( -19.99999999999849720, -20.00000000000000000, 6.500000000004389378 ) ) ;
#795=PRODUCT_DEFINITION_FORMATION_WITH_SPECIFIED_SOURCE ( 'ANY', '', #3402, .NOT_KNOWN. ) ;
#835=EDGE_LOOP ( 'NONE', ( #18572, #6387, #5967, #11547 ) ) ;
#955=EDGE_LOOP ( 'NONE', ( #3394, #13500, #9545, #120 ) ) ;
#1045=ORIENTED_EDGE ( 'NONE', *, *, #7237, .F. ) ;
#1151=CARTESIAN_POINT ( 'NONE',  ( -19.99999998251385591, -22.62500000000000000, -8.249999999995454303 ) ) ;
#1225=ORIENTED_EDGE ( 'NONE', *, *, #8827, .T. ) ;
#1423=DIRECTION ( 'NONE',  ( -2.269700743865584947E-13, -2.220446049247695246E-15, -1.000000000000000000 ) ) ;
#1588=AXIS2_PLACEMENT_3D ( 'NONE', #7935, #15165, #20643 ) ;
#1618=CONICAL_SURFACE ( 'NONE', #20970, 2.624999999999998668, 0.4636476090008101458 ) ;
#1660=DIRECTION ( 'NONE',  ( -6.662111338785949120E-09, 1.000000000000000000, -1.982541115402066096E-15 ) ) ;
#1682=EDGE_CURVE ( 'NONE', #22814, #7235, #5366, .T. ) ;
#1700=CARTESIAN_POINT ( 'NONE',  ( -20.00000000000190070, -20.00000000000000000, -8.499999999995459632 ) ) ;
#1720=ORIENTED_EDGE ( 'NONE', *, *, #8269, .T. ) ;
#1803=CARTESIAN_POINT ( 'NONE',  ( -19.99999999999819877, -20.00000000000000000, 8.000000000004540368 ) ) ;
#1840=ORIENTED_EDGE ( 'NONE', *, *, #16144, .T. ) ;
#2041=ORIENTED_EDGE ( 'NONE', *, *, #19548, .F. ) ;
#2050=DIRECTION ( 'NONE',  ( -2.269700743865584947E-13, -2.220446049247695246E-15, -1.000000000000000000 ) ) ;
#2095=ORIENTED_EDGE ( 'NONE', *, *, #14638, .T. ) ;
#2347=VERTEX_POINT ( 'NONE', #5753 ) ;
#2474=ADVANCED_FACE ( 'NONE', ( #44 ), #21786, .T. ) ;
#2524=AXIS2_PLACEMENT_3D ( 'NONE', #13314, #15206, #16868 ) ;
#2569=CARTESIAN_POINT ( 'NONE',  ( 0.000000000000000000, 0.000000000000000000, 0.000000000000000000 ) ) ;
#2730=CARTESIAN_POINT ( 'NONE',  ( -20.00000000000149925, -20.00000000000000000, -6.499999999995289990 ) ) ;
#2793=CARTESIAN_POINT ( 'NONE',  ( -19.99999999999809930, -20.00000000000000000, 8.500000000004551026 ) ) ;
#2921=CARTESIAN_POINT ( 'NONE',  ( -20.00000000000180123, -20.00000000000000000, -7.999999999995458744 ) ) ;
#2949=ORIENTED_EDGE ( 'NONE', *, *, #15007, .F. ) ;
#2950=VERTEX_POINT ( 'NONE', #16291 ) ;
#2994=DIRECTION ( 'NONE',  ( -6.662111519016958720E-09, 1.000000000000000000, -2.523234146875356491E-15 ) ) ;
#3065=EDGE_CURVE ( 'NONE', #22508, #12435, #7102, .T. ) ;
#3126=CONICAL_SURFACE ( 'NONE', #1588, 2.624999999999998668, 0.4636476090008101458 ) ;
#3158=DIRECTION ( 'NONE',  ( -2.269700743865584947E-13, -2.220446049247695246E-15, -1.000000000000000000 ) ) ;
#3201=VERTEX_POINT ( 'NONE', #5099 ) ;
#3322=AXIS2_PLACEMENT_3D ( 'NONE', #715, #15218, #6208 ) ;
#3363=CLOSED_SHELL ( 'NONE', ( #10547, #14906, #16759, #535, #19936, #7806, #206, #2474, #9481, #12393 ) ) ;
#3394=ORIENTED_EDGE ( 'NONE', *, *, #10947, .T. ) ;
#3402=PRODUCT ( '1602p_c_18', '1602p_c_18', '', ( #5974 ) ) ;
#3525=SPHERICAL_SURFACE ( 'NONE', #13960, 15.25000000000000000 ) ;
#3575=DIRECTION ( 'NONE',  ( 2.269700743865589996E-13, 2.220446049247695246E-15, 1.000000000000000000 ) ) ;
#3669=AXIS2_PLACEMENT_3D ( 'NONE', #13327, #5958, #13100 ) ;
#3673=DIRECTION ( 'NONE',  ( -6.662111519016958720E-09, 1.000000000000000000, -2.523234146875356491E-15 ) ) ;
#3749=DIRECTION ( 'NONE',  ( 1.000000000000000000, 0.000000000000000000, 0.000000000000000000 ) ) ;
#3852=CARTESIAN_POINT ( 'NONE',  ( -20.00000000000000000, -20.00000000000000000, 4.543842380125470691E-12 ) ) ;
#3890=CIRCLE ( 'NONE', #10752, 2.749999999999999112 ) ;
#3908=CARTESIAN_POINT ( 'NONE',  ( -19.99999998251005806, -22.50000000000000000, 8.000000000004545697 ) ) ;
#3942=ORIENTED_EDGE ( 'NONE', *, *, #4032, .T. ) ;
#3948=DIRECTION ( 'NONE',  ( -1.000000000000000000, 2.275047181608927151E-16, 0.000000000000000000 ) ) ;
#3977=EDGE_LOOP ( 'NONE', ( #16493, #18923, #18510, #7046 ) ) ;
#4032=EDGE_CURVE ( 'NONE', #2950, #7235, #3890, .T. ) ;
#4137=CARTESIAN_POINT ( 'NONE',  ( -20.00000000000149925, -20.00000000000000000, 8.750000000004709122 ) ) ;
#4214=DIRECTION ( 'NONE',  ( -2.269700743865584947E-13, -2.220446049247695246E-15, -1.000000000000000000 ) ) ;
#4280=ORIENTED_EDGE ( 'NONE', *, *, #17496, .F. ) ;
#4418=CARTESIAN_POINT ( 'NONE',  ( -20.00000001748994549, -17.37500000000000000, -8.249999999995464961 ) ) ;
#4458=CIRCLE ( 'NONE', #20370, 2.499999999999998668 ) ;
#4536=CARTESIAN_POINT ( 'NONE',  ( -20.00000001832276553, -17.25000000000000000, -8.499999999995466737 ) ) ;
#4719=ORIENTED_EDGE ( 'NONE', *, *, #5990, .T. ) ;
#4788=( NAMED_UNIT ( * ) SI_UNIT ( $, .STERADIAN. ) SOLID_ANGLE_UNIT ( ) );
#4804=LINE ( 'NONE', #12074, #8319 ) ;
#4889=DIRECTION ( 'NONE',  ( -2.979184025347991663E-09, 0.4472135954999659213, 0.8944271909999118586 ) ) ;
#4899=SHAPE_DEFINITION_REPRESENTATION ( #5301, #12037 ) ;
#4933=DIRECTION ( 'NONE',  ( -6.662112528310618598E-09, 1.000000000000000000, -2.081668171172169697E-15 ) ) ;
#4935=DIRECTION ( 'NONE',  ( -6.662112528310618598E-09, 1.000000000000000000, -2.081668171172169697E-15 ) ) ;
#4982=AXIS2_PLACEMENT_3D ( 'NONE', #3852, #7319, #14559 ) ;
#4994=FACE_OUTER_BOUND ( 'NONE', #12590, .T. ) ;
#5013=DIRECTION ( 'NONE',  ( 1.224646799147353207E-16, 1.000000000000000000, -0.000000000000000000 ) ) ;
#5047=DIRECTION ( 'NONE',  ( -2.269700743865584947E-13, -2.220446049247695246E-15, -1.000000000000000000 ) ) ;
#5064=CARTESIAN_POINT ( 'NONE',  ( -20.00000000000180123, -20.00000000000000000, -7.999999999995458744 ) ) ;
#5086=ORIENTED_EDGE ( 'NONE', *, *, #351, .T. ) ;
#5099=CARTESIAN_POINT ( 'NONE',  ( -22.74999999999852918, -20.00000000000000000, 8.500000000005176304 ) ) ;
#5267=CARTESIAN_POINT ( 'NONE',  ( -20.00000001665708282, -17.50000000000000000, -7.999999999995464073 ) ) ;
#5276=CYLINDRICAL_SURFACE ( 'NONE', #22276, 2.499999999999998668 ) ;
#5301=PRODUCT_DEFINITION_SHAPE ( 'NONE', 'NONE',  #6763 ) ;
#5366=LINE ( 'NONE', #9523, #18988 ) ;
#5372=DIRECTION ( 'NONE',  ( -6.662111338785949120E-09, 1.000000000000000000, -1.982541115402066096E-15 ) ) ;
#5497=CIRCLE ( 'NONE', #14600, 15.25000000000000000 ) ;
#5589=CIRCLE ( 'NONE', #8639, 2.749999999999999112 ) ;
#5639=EDGE_CURVE ( 'NONE', #22814, #21354, #4804, .T. ) ;
#5656=ORIENTED_EDGE ( 'NONE', *, *, #16144, .F. ) ;
#5668=EDGE_LOOP ( 'NONE', ( #12889, #2095, #17613, #4719 ) ) ;
#5683=ORIENTED_EDGE ( 'NONE', *, *, #21420, .T. ) ;
#5701=DIRECTION ( 'NONE',  ( 0.000000000000000000, 1.000000000000000000, 0.000000000000000000 ) ) ;
#5753=CARTESIAN_POINT ( 'NONE',  ( -20.00000001831885044, -17.24999999999999645, 8.500000000004543921 ) ) ;
#5868=CARTESIAN_POINT ( 'NONE',  ( -19.99999999999849720, -20.00000000000000000, -8.749999999995610622 ) ) ;
#5874=DIRECTION ( 'NONE',  ( -2.269700743865584947E-13, -2.220446049247695246E-15, -1.000000000000000000 ) ) ;
#5889=ORIENTED_EDGE ( 'NONE', *, *, #19486, .T. ) ;
#5958=DIRECTION ( 'NONE',  ( -2.269700743865584947E-13, -2.220446049247695246E-15, -1.000000000000000000 ) ) ;
#5967=ORIENTED_EDGE ( 'NONE', *, *, #14610, .T. ) ;
#5974=MECHANICAL_CONTEXT ( 'NONE', #608, 'mechanical' ) ;
#5990=EDGE_CURVE ( 'NONE', #20926, #12435, #714, .T. ) ;
#5996=DIRECTION ( 'NONE',  ( -6.662111519016958720E-09, 1.000000000000000000, -2.523234146875356491E-15 ) ) ;
#6022=VERTEX_POINT ( 'NONE', #4536 ) ;
#6208=DIRECTION ( 'NONE',  ( 0.000000000000000000, 0.000000000000000000, -1.000000000000000000 ) ) ;
#6238=DIRECTION ( 'NONE',  ( 1.000000000000000000, 0.000000000000000000, 0.000000000000000000 ) ) ;
#6375=AXIS2_PLACEMENT_3D ( 'NONE', #2921, #12326, #4935 ) ;
#6387=ORIENTED_EDGE ( 'NONE', *, *, #3065, .T. ) ;
#6388=DIRECTION ( 'NONE',  ( 0.000000000000000000, -1.000000000000000000, 0.000000000000000000 ) ) ;
#6436=ORIENTED_EDGE ( 'NONE', *, *, #7237, .T. ) ;
#6657=DIRECTION ( 'NONE',  ( 1.000000000000000000, 0.000000000000000000, 0.000000000000000000 ) ) ;
#6763=PRODUCT_DEFINITION ( 'UNKNOWN', '', #795, #21787 ) ;
#6872=DIRECTION ( 'NONE',  ( 2.979184080115845427E-09, -0.4472135954999635343, -0.8944271909999130798 ) ) ;
#7046=ORIENTED_EDGE ( 'NONE', *, *, #16572, .F. ) ;
#7089=CARTESIAN_POINT ( 'NONE',  ( -20.00000001665348037, -17.50000000000000000, 8.000000000004535039 ) ) ;
#7102=CIRCLE ( 'NONE', #8619, 15.25000000000000000 ) ;
#7136=CIRCLE ( 'NONE', #6375, 2.499999999999998668 ) ;
#7173=CARTESIAN_POINT ( 'NONE',  ( -20.00000000000190070, -20.00000000000000000, -8.499999999995459632 ) ) ;
#7235=VERTEX_POINT ( 'NONE', #12202 ) ;
#7237=EDGE_CURVE ( 'NONE', #22814, #10370, #15665, .T. ) ;
#7319=DIRECTION ( 'NONE',  ( -2.269700743865584947E-13, -2.220446049247695246E-15, -1.000000000000000000 ) ) ;
#7650=CARTESIAN_POINT ( 'NONE',  ( -22.75000000000231637, -20.00000000000000000, -8.499999999994834354 ) ) ;
#7706=CIRCLE ( 'NONE', #8853, 2.749999999999999112 ) ;
#7806=ADVANCED_FACE ( 'NONE', ( #4994 ), #1618, .T. ) ;
#7935=CARTESIAN_POINT ( 'NONE',  ( -20.00000000000190070, -20.00000000000000000, -8.249999999995459632 ) ) ;
#8076=DIRECTION ( 'NONE',  ( 1.224646799147353207E-16, 1.000000000000000000, -0.000000000000000000 ) ) ;
#8269=EDGE_CURVE ( 'NONE', #21354, #20926, #10211, .T. ) ;
#8276=DIRECTION ( 'NONE',  ( -6.662112528310618598E-09, 1.000000000000000000, -2.081668171172169697E-15 ) ) ;
#8319=VECTOR ( 'NONE', #5047, 1000.000000000000000 ) ;
#8343=DIRECTION ( 'NONE',  ( -2.269700743865584947E-13, -2.220446049247695246E-15, -1.000000000000000000 ) ) ;
#8482=VECTOR ( 'NONE', #8343, 1000.000000000000000 ) ;
#8483=AXIS2_PLACEMENT_3D ( 'NONE', #10264, #19276, #2994 ) ;
#8619=AXIS2_PLACEMENT_3D ( 'NONE', #11221, #8076, #3948 ) ;
#8639=AXIS2_PLACEMENT_3D ( 'NONE', #19843, #1423, #3673 ) ;
#8646=ORIENTED_EDGE ( 'NONE', *, *, #1682, .T. ) ;
#8827=EDGE_CURVE ( 'NONE', #20679, #21354, #16092, .T. ) ;
#8853=AXIS2_PLACEMENT_3D ( 'NONE', #15191, #21950, #13429 ) ;
#9161=SPHERICAL_SURFACE ( 'NONE', #22933, 15.25000000000000000 ) ;
#9209=FACE_OUTER_BOUND ( 'NONE', #955, .T. ) ;
#9223=ORIENTED_EDGE ( 'NONE', *, *, #21420, .F. ) ;
#9281=ORIENTED_EDGE ( 'NONE', *, *, #16572, .T. ) ;
#9328=AXIS2_PLACEMENT_3D ( 'NONE', #22495, #9442, #6238 ) ;
#9421=LINE ( 'NONE', #4418, #15655 ) ;
#9442=DIRECTION ( 'NONE',  ( 0.000000000000000000, 1.000000000000000000, 0.000000000000000000 ) ) ;
#9481=ADVANCED_FACE ( 'NONE', ( #21867 ), #12909, .T. ) ;
#9523=CARTESIAN_POINT ( 'NONE',  ( -19.99999998251005806, -22.62500000000000000, 8.250000000004556355 ) ) ;
#9545=ORIENTED_EDGE ( 'NONE', *, *, #8827, .F. ) ;
#9975=DIRECTION ( 'NONE',  ( 0.000000000000000000, 0.000000000000000000, -1.000000000000000000 ) ) ;
#10129=EDGE_LOOP ( 'NONE', ( #1225, #1720, #12742, #2949, #5656 ) ) ;
#10142=DIRECTION ( 'NONE',  ( -1.000000000000000000, 2.275047181608926658E-16, 0.000000000000000000 ) ) ;
#10211=LINE ( 'NONE', #1151, #15289 ) ;
#10264=CARTESIAN_POINT ( 'NONE',  ( -19.99999999999809930, -20.00000000000000000, 8.500000000004551026 ) ) ;
#10370=VERTEX_POINT ( 'NONE', #7089 ) ;
#10450=CARTESIAN_POINT ( 'NONE',  ( -20.00000000000149925, -20.00000000000000000, -6.499999999995289990 ) ) ;
#10534=CARTESIAN_POINT ( 'NONE',  ( -19.99999999999819877, -20.00000000000000000, 8.000000000004540368 ) ) ;
#10547=ADVANCED_FACE ( 'NONE', ( #9209 ), #45, .T. ) ;
#10672=DIRECTION ( 'NONE',  ( 0.000000000000000000, 1.000000000000000000, 0.000000000000000000 ) ) ;
#10724=EDGE_LOOP ( 'NONE', ( #1045, #8646, #5683, #16277, #4280 ) ) ;
#10752=AXIS2_PLACEMENT_3D ( 'NONE', #2793, #4214, #5996 ) ;
#10947=EDGE_CURVE ( 'NONE', #10370, #22814, #4458, .T. ) ;
#10986=EDGE_CURVE ( 'NONE', #21478, #20926, #16199, .T. ) ;
#11221=CARTESIAN_POINT ( 'NONE',  ( -19.99999999999849720, -20.00000000000000000, 6.500000000004389378 ) ) ;
#11424=ORIENTED_EDGE ( 'NONE', *, *, #5990, .F. ) ;
#11547=ORIENTED_EDGE ( 'NONE', *, *, #15007, .T. ) ;
#11667=ADVANCED_BREP_SHAPE_REPRESENTATION ( '', ( #17588, #12739 ), #20713 ) ;
#11820=SHAPE_REPRESENTATION_RELATIONSHIP ( 'NONE' , 'NONE' ,  #12037, #11667 ) ;
#12037=SHAPE_REPRESENTATION ( '1602p_c_18', ( #12739 ), #20713 ) ;
#12074=CARTESIAN_POINT ( 'NONE',  ( -19.99999998334471840, -22.50000000000000000, 4.549393491468339877E-12 ) ) ;
#12156=CARTESIAN_POINT ( 'NONE',  ( -20.00000001665528160, -17.50000000000000000, 4.538291268782600698E-12 ) ) ;
#12191=EDGE_CURVE ( 'NONE', #21354, #20679, #7136, .T. ) ;
#12202=CARTESIAN_POINT ( 'NONE',  ( -19.99999998167723803, -22.75000000000000000, 8.500000000004558132 ) ) ;
#12322=AXIS2_PLACEMENT_3D ( 'NONE', #5064, #21438, #8276 ) ;
#12326=DIRECTION ( 'NONE',  ( -2.269700743865589996E-13, -2.220446049247695246E-15, -1.000000000000000000 ) ) ;
#12393=ADVANCED_FACE ( 'NONE', ( #21540 ), #5276, .T. ) ;
#12435=VERTEX_POINT ( 'NONE', #7650 ) ;
#12590=EDGE_LOOP ( 'NONE', ( #21269, #15414, #1840, #22755, #11424 ) ) ;
#12739=AXIS2_PLACEMENT_3D ( 'NONE', #2569, #13380, #415 ) ;
#12742=ORIENTED_EDGE ( 'NONE', *, *, #10986, .F. ) ;
#12841=FACE_OUTER_BOUND ( 'NONE', #5668, .T. ) ;
#12889=ORIENTED_EDGE ( 'NONE', *, *, #3065, .F. ) ;
#12909=CONICAL_SURFACE ( 'NONE', #22748, 2.624999999999998668, 0.4636476090008128104 ) ;
#13100=DIRECTION ( 'NONE',  ( -6.662111519016958720E-09, 1.000000000000000000, -2.523234146875356491E-15 ) ) ;
#13176=AXIS2_PLACEMENT_3D ( 'NONE', #7173, #21519, #248 ) ;
#13250=ORIENTED_EDGE ( 'NONE', *, *, #12191, .F. ) ;
#13314=CARTESIAN_POINT ( 'NONE',  ( -19.99999999999809930, -20.00000000000000000, 8.500000000004551026 ) ) ;
#13327=CARTESIAN_POINT ( 'NONE',  ( -20.00000000000190070, -20.00000000000000000, -8.499999999995459632 ) ) ;
#13380=DIRECTION ( 'NONE',  ( 0.000000000000000000, 0.000000000000000000, 1.000000000000000000 ) ) ;
#13429=DIRECTION ( 'NONE',  ( -6.662111519016958720E-09, 1.000000000000000000, -2.523234146875356491E-15 ) ) ;
#13440=CARTESIAN_POINT ( 'NONE',  ( -19.99999998251385946, -22.50000000000000000, -7.999999999995453415 ) ) ;
#13500=ORIENTED_EDGE ( 'NONE', *, *, #5639, .T. ) ;
#13531=FACE_OUTER_BOUND ( 'NONE', #3977, .T. ) ;
#13960=AXIS2_PLACEMENT_3D ( 'NONE', #21343, #10672, #3749 ) ;
#14135=DIRECTION ( 'NONE',  ( -2.269700743865584947E-13, -2.220446049247695246E-15, -1.000000000000000000 ) ) ;
#14155=ORIENTED_EDGE ( 'NONE', *, *, #5639, .F. ) ;
#14559=DIRECTION ( 'NONE',  ( -6.662112528310618598E-09, 1.000000000000000000, -2.220444537147720967E-15 ) ) ;
#14600=AXIS2_PLACEMENT_3D ( 'NONE', #10450, #6388, #9975 ) ;
#14610=EDGE_CURVE ( 'NONE', #12435, #6022, #15413, .T. ) ;
#14629=DIRECTION ( 'NONE',  ( 2.979589986992270586E-09, -0.4472135954999619800, 0.8944271909999139680 ) ) ;
#14638=EDGE_CURVE ( 'NONE', #22508, #21478, #18880, .T. ) ;
#14771=( LENGTH_UNIT ( ) NAMED_UNIT ( * ) SI_UNIT ( .MILLI., .METRE. ) );
#14773=DIRECTION ( 'NONE',  ( -6.662112528310618598E-09, 1.000000000000000000, -2.220444537147720967E-15 ) ) ;
#14848=DIRECTION ( 'NONE',  ( 1.000000000000000000, 0.000000000000000000, 0.000000000000000000 ) ) ;
#14906=ADVANCED_FACE ( 'NONE', ( #19718 ), #19629, .T. ) ;
#15007=EDGE_CURVE ( 'NONE', #6022, #21478, #5589, .T. ) ;
#15028=CIRCLE ( 'NONE', #2524, 2.749999999999999112 ) ;
#15039=ORIENTED_EDGE ( 'NONE', *, *, #4032, .F. ) ;
#15165=DIRECTION ( 'NONE',  ( -2.269700743865584947E-13, -2.220446049247695246E-15, -1.000000000000000000 ) ) ;
#15191=CARTESIAN_POINT ( 'NONE',  ( -19.99999999999809930, -20.00000000000000000, 8.500000000004551026 ) ) ;
#15206=DIRECTION ( 'NONE',  ( -2.269700743865584947E-13, -2.220446049247695246E-15, -1.000000000000000000 ) ) ;
#15218=DIRECTION ( 'NONE',  ( 0.000000000000000000, -1.000000000000000000, 0.000000000000000000 ) ) ;
#15287=AXIS2_PLACEMENT_3D ( 'NONE', #10534, #3158, #4933 ) ;
#15289=VECTOR ( 'NONE', #6872, 1000.000000000000114 ) ;
#15296=VECTOR ( 'NONE', #4889, 1000.000000000000000 ) ;
#15413=CIRCLE ( 'NONE', #3669, 2.749999999999999112 ) ;
#15414=ORIENTED_EDGE ( 'NONE', *, *, #12191, .T. ) ;
#15438=AXIS2_PLACEMENT_3D ( 'NONE', #17952, #3575, #1660 ) ;
#15655=VECTOR ( 'NONE', #495, 1000.000000000000000 ) ;
#15665=CIRCLE ( 'NONE', #15287, 2.499999999999998668 ) ;
#15843=UNCERTAINTY_MEASURE_WITH_UNIT (LENGTH_MEASURE( 1.000000000000000082E-05 ), #14771, 'distance_accuracy_value', 'NONE');
#16092=CIRCLE ( 'NONE', #12322, 2.499999999999998668 ) ;
#16144=EDGE_CURVE ( 'NONE', #20679, #6022, #9421, .T. ) ;
#16199=CIRCLE ( 'NONE', #13176, 2.749999999999999112 ) ;
#16226=ORIENTED_EDGE ( 'NONE', *, *, #1682, .F. ) ;
#16277=ORIENTED_EDGE ( 'NONE', *, *, #21002, .T. ) ;
#16291=CARTESIAN_POINT ( 'NONE',  ( -17.24999999999766587, -20.00000000000000000, 8.500000000003927525 ) ) ;
#16300=DIRECTION ( 'NONE',  ( -2.269700743865584947E-13, -2.220446049247695246E-15, -1.000000000000000000 ) ) ;
#16493=ORIENTED_EDGE ( 'NONE', *, *, #21002, .F. ) ;
#16520=DIRECTION ( 'NONE',  ( 2.269700743865589996E-13, 2.220446049247695246E-15, 1.000000000000000000 ) ) ;
#16572=EDGE_CURVE ( 'NONE', #2347, #2950, #7706, .T. ) ;
#16653=( NAMED_UNIT ( * ) PLANE_ANGLE_UNIT ( ) SI_UNIT ( $, .RADIAN. ) );
#16759=ADVANCED_FACE ( 'NONE', ( #13531 ), #22660, .T. ) ;
#16791=CARTESIAN_POINT ( 'NONE',  ( -20.00000000000000000, -20.00000000000000000, 4.543842380125470691E-12 ) ) ;
#16868=DIRECTION ( 'NONE',  ( -6.662111519016958720E-09, 1.000000000000000000, -2.523234146875356491E-15 ) ) ;
#17014=CARTESIAN_POINT ( 'NONE',  ( -19.99999998168114601, -22.75000000000000000, -8.499999999995452526 ) ) ;
#17129=EDGE_LOOP ( 'NONE', ( #14155, #6436, #5889, #13250 ) ) ;
#17375=CARTESIAN_POINT ( 'NONE',  ( -20.00000000000149925, -20.00000000000000000, -6.499999999995289990 ) ) ;
#17496=EDGE_CURVE ( 'NONE', #10370, #2347, #21261, .T. ) ;
#17588=MANIFOLD_SOLID_BREP ( 'Imported1', #3363 ) ;
#17613=ORIENTED_EDGE ( 'NONE', *, *, #10986, .T. ) ;
#17848=ORIENTED_EDGE ( 'NONE', *, *, #17496, .T. ) ;
#17852=CARTESIAN_POINT ( 'NONE',  ( -19.99999999999809930, -20.00000000000000000, 8.250000000004551026 ) ) ;
#17952=CARTESIAN_POINT ( 'NONE',  ( -19.99999999999809930, -20.00000000000000000, 8.250000000004551026 ) ) ;
#18033=CARTESIAN_POINT ( 'NONE',  ( -17.25000000000148503, -20.00000000000000000, -8.499999999996081357 ) ) ;
#18312=CARTESIAN_POINT ( 'NONE',  ( -19.99999999999849720, -20.00000000000000000, 6.500000000004389378 ) ) ;
#18510=ORIENTED_EDGE ( 'NONE', *, *, #351, .F. ) ;
#18572=ORIENTED_EDGE ( 'NONE', *, *, #14638, .F. ) ;
#18880=CIRCLE ( 'NONE', #3322, 15.25000000000000000 ) ;
#18923=ORIENTED_EDGE ( 'NONE', *, *, #19548, .T. ) ;
#18988=VECTOR ( 'NONE', #14629, 999.9999999999998863 ) ;
#19210=FACE_OUTER_BOUND ( 'NONE', #10129, .T. ) ;
#19276=DIRECTION ( 'NONE',  ( -2.269700743865584947E-13, -2.220446049247695246E-15, -1.000000000000000000 ) ) ;
#19486=EDGE_CURVE ( 'NONE', #10370, #20679, #19504, .T. ) ;
#19504=LINE ( 'NONE', #12156, #8482 ) ;
#19548=EDGE_CURVE ( 'NONE', #3201, #23008, #22500, .T. ) ;
#19629=CONICAL_SURFACE ( 'NONE', #15438, 2.624999999999998668, 0.4636476090008128104 ) ;
#19718=FACE_OUTER_BOUND ( 'NONE', #10724, .T. ) ;
#19751=DIRECTION ( 'NONE',  ( -6.662112528310618598E-09, 1.000000000000000000, -2.081668171172169697E-15 ) ) ;
#19843=CARTESIAN_POINT ( 'NONE',  ( -20.00000000000190070, -20.00000000000000000, -8.499999999995459632 ) ) ;
#19849=CIRCLE ( 'NONE', #8483, 2.749999999999999112 ) ;
#19936=ADVANCED_FACE ( 'NONE', ( #19210 ), #3126, .T. ) ;
#20105=DIRECTION ( 'NONE',  ( -6.662111519016958720E-09, 1.000000000000000000, -2.523234146875356491E-15 ) ) ;
#20190=ORIENTED_EDGE ( 'NONE', *, *, #10947, .F. ) ;
#20236=AXIS2_PLACEMENT_3D ( 'NONE', #17375, #5013, #10142 ) ;
#20370=AXIS2_PLACEMENT_3D ( 'NONE', #1803, #2050, #19751 ) ;
#20466=AXIS2_PLACEMENT_3D ( 'NONE', #1700, #16300, #20105 ) ;
#20643=DIRECTION ( 'NONE',  ( -6.662111338785949120E-09, 1.000000000000000000, -1.982541115402066096E-15 ) ) ;
#20679=VERTEX_POINT ( 'NONE', #5267 ) ;
#20713=( GEOMETRIC_REPRESENTATION_CONTEXT ( 3 ) GLOBAL_UNCERTAINTY_ASSIGNED_CONTEXT ( ( #15843 ) ) GLOBAL_UNIT_ASSIGNED_CONTEXT ( ( #14771, #16653, #4788 ) ) REPRESENTATION_CONTEXT ( 'NONE', 'WORKASPACE' ) );
#20926=VERTEX_POINT ( 'NONE', #17014 ) ;
#20970=AXIS2_PLACEMENT_3D ( 'NONE', #23139, #14135, #21379 ) ;
#21002=EDGE_CURVE ( 'NONE', #3201, #2347, #19849, .T. ) ;
#21018=DIRECTION ( 'NONE',  ( 0.000000000000000000, 1.000000000000000000, 0.000000000000000000 ) ) ;
#21261=LINE ( 'NONE', #23150, #15296 ) ;
#21269=ORIENTED_EDGE ( 'NONE', *, *, #8269, .F. ) ;
#21343=CARTESIAN_POINT ( 'NONE',  ( -19.99999999999849720, -20.00000000000000000, 6.500000000004389378 ) ) ;
#21350=AXIS2_PLACEMENT_3D ( 'NONE', #2730, #21018, #6657 ) ;
#21354=VERTEX_POINT ( 'NONE', #13440 ) ;
#21379=DIRECTION ( 'NONE',  ( -6.662111338785949120E-09, 1.000000000000000000, -1.982541115402066096E-15 ) ) ;
#21420=EDGE_CURVE ( 'NONE', #7235, #3201, #15028, .T. ) ;
#21438=DIRECTION ( 'NONE',  ( -2.269700743865589996E-13, -2.220446049247695246E-15, -1.000000000000000000 ) ) ;
#21478=VERTEX_POINT ( 'NONE', #18033 ) ;
#21519=DIRECTION ( 'NONE',  ( -2.269700743865584947E-13, -2.220446049247695246E-15, -1.000000000000000000 ) ) ;
#21540=FACE_OUTER_BOUND ( 'NONE', #17129, .T. ) ;
#21786=SPHERICAL_SURFACE ( 'NONE', #9328, 15.25000000000000000 ) ;
#21787=DESIGN_CONTEXT ( 'detailed design', #22188, 'design' ) ;
#21812=EDGE_LOOP ( 'NONE', ( #16226, #20190, #17848, #9281, #3942 ) ) ;
#21867=FACE_OUTER_BOUND ( 'NONE', #21812, .T. ) ;
#21950=DIRECTION ( 'NONE',  ( -2.269700743865584947E-13, -2.220446049247695246E-15, -1.000000000000000000 ) ) ;
#22188=APPLICATION_CONTEXT ( 'configuration controlled 3d designs of mechanical parts and assemblies' ) ;
#22276=AXIS2_PLACEMENT_3D ( 'NONE', #16791, #5874, #14773 ) ;
#22495=CARTESIAN_POINT ( 'NONE',  ( -20.00000000000149925, -20.00000000000000000, -6.499999999995289990 ) ) ;
#22500=CIRCLE ( 'NONE', #20236, 15.25000000000000355 ) ;
#22508=VERTEX_POINT ( 'NONE', #5868 ) ;
#22660=SPHERICAL_SURFACE ( 'NONE', #21350, 15.25000000000000000 ) ;
#22748=AXIS2_PLACEMENT_3D ( 'NONE', #17852, #16520, #5372 ) ;
#22755=ORIENTED_EDGE ( 'NONE', *, *, #14610, .F. ) ;
#22814=VERTEX_POINT ( 'NONE', #3908 ) ;
#22933=AXIS2_PLACEMENT_3D ( 'NONE', #18312, #5701, #14848 ) ;
#23008=VERTEX_POINT ( 'NONE', #4137 ) ;
#23139=CARTESIAN_POINT ( 'NONE',  ( -20.00000000000190070, -20.00000000000000000, -8.249999999995459632 ) ) ;
#23150=CARTESIAN_POINT ( 'NONE',  ( -20.00000001748614054, -17.37500000000000000, 8.250000000004545697 ) ) ;
#23459=FACE_OUTER_BOUND ( 'NONE', #835, .T. ) ;
#23550=COLOUR_RGB('Black', 0.08235294, 0.09019608, 0.10196078);
#23551=FILL_AREA_STYLE_COLOUR('',#23550);
#23552=FILL_AREA_STYLE('',(#23551));
#23553=SURFACE_STYLE_FILL_AREA(#23552);
#23554=SURFACE_SIDE_STYLE('',(#23553));
#23555=SURFACE_STYLE_USAGE(.BOTH.,#23554);
#23556=PRESENTATION_STYLE_ASSIGNMENT((#23555));
#23589=STYLED_ITEM('',(#23556),#17588);
#23590=MECHANICAL_DESIGN_GEOMETRIC_PRESENTATION_REPRESENTATION('',(#23589),#20713);
ENDSEC;
END-ISO-10303-21;
